ISO-10303-21;
HEADER;
/* Generated by software containing ST-Developer
 * from STEP Tools, Inc. (www.steptools.com) 
 */

FILE_DESCRIPTION(
/* description */ ('Over-Centre Plunger Toggle Clamp on Slotted Fixture Frame'),
/* implementation_level */ '2;1');

FILE_NAME(
/* name */ 
'Captive slot nut.step',
/* time_stamp */ '2026-10-28T03:23:24-07:00',
/* author */ (''),
/* organization */ (''),
/* preprocessor_version */ 'ST-DEVELOPER v20.2',
/* originating_system */ 'Autodesk Translation Framework v15.17.0.0',
/* authorisation */ '');

FILE_SCHEMA (('AUTOMOTIVE_DESIGN { 1 0 10303 214 3 1 1 }'));
ENDSEC;

DATA;
#10=MECHANICAL_DESIGN_GEOMETRIC_PRESENTATION_REPRESENTATION('',(#526),#15212);
#427=ELLIPSE('',#9119,0.299389011154384,0.2117);
#428=ELLIPSE('',#9123,0.299389011154384,0.2117);
#442=SHAPE_REPRESENTATION_RELATIONSHIP('SRR','None',#15416,#484);
#484=ADVANCED_BREP_SHAPE_REPRESENTATION('',(#577),#15178);
#526=STYLED_ITEM('',(#15726),#577);
#577=MANIFOLD_SOLID_BREP('Body1',#8258);
#716=FACE_BOUND('',#1877,.T.);
#912=PLANE('',#9109);
#913=PLANE('',#9110);
#914=PLANE('',#9111);
#915=PLANE('',#9113);
#916=PLANE('',#9114);
#917=PLANE('',#9115);
#918=PLANE('',#9116);
#919=PLANE('',#9117);
#920=PLANE('',#9118);
#921=PLANE('',#9125);
#922=PLANE('',#9126);
#923=PLANE('',#9127);
#924=PLANE('',#9128);
#1283=FACE_OUTER_BOUND('',#1874,.T.);
#1284=FACE_OUTER_BOUND('',#1875,.T.);
#1285=FACE_OUTER_BOUND('',#1876,.T.);
#1286=FACE_OUTER_BOUND('',#1878,.T.);
#1287=FACE_OUTER_BOUND('',#1879,.T.);
#1288=FACE_OUTER_BOUND('',#1880,.T.);
#1289=FACE_OUTER_BOUND('',#1881,.T.);
#1290=FACE_OUTER_BOUND('',#1882,.T.);
#1291=FACE_OUTER_BOUND('',#1883,.T.);
#1292=FACE_OUTER_BOUND('',#1884,.T.);
#1293=FACE_OUTER_BOUND('',#1885,.T.);
#1294=FACE_OUTER_BOUND('',#1886,.T.);
#1295=FACE_OUTER_BOUND('',#1887,.T.);
#1296=FACE_OUTER_BOUND('',#1888,.T.);
#1874=EDGE_LOOP('',(#6475,#6476,#6477,#6478));
#1875=EDGE_LOOP('',(#6479,#6480,#6481,#6482));
#1876=EDGE_LOOP('',(#6483,#6484,#6485,#6486));
#1877=EDGE_LOOP('',(#6487));
#1878=EDGE_LOOP('',(#6488,#6489,#6490,#6491,#6492,#6493,#6494,#6495,#6496,
#6497));
#1879=EDGE_LOOP('',(#6498,#6499,#6500,#6501));
#1880=EDGE_LOOP('',(#6502,#6503,#6504,#6505));
#1881=EDGE_LOOP('',(#6506,#6507,#6508,#6509,#6510,#6511,#6512,#6513,#6514,
#6515));
#1882=EDGE_LOOP('',(#6516,#6517,#6518,#6519));
#1883=EDGE_LOOP('',(#6520,#6521,#6522,#6523,#6524,#6525));
#1884=EDGE_LOOP('',(#6526,#6527,#6528,#6529,#6530,#6531,#6532,#6533));
#1885=EDGE_LOOP('',(#6534,#6535,#6536,#6537,#6538));
#1886=EDGE_LOOP('',(#6539,#6540,#6541,#6542));
#1887=EDGE_LOOP('',(#6543,#6544,#6545,#6546,#6547,#6548));
#1888=EDGE_LOOP('',(#6549,#6550,#6551,#6552));
#2550=LINE('',#13336,#3180);
#2551=LINE('',#13338,#3181);
#2552=LINE('',#13340,#3182);
#2553=LINE('',#13341,#3183);
#2554=LINE('',#13344,#3184);
#2555=LINE('',#13346,#3185);
#2556=LINE('',#13347,#3186);
#2557=LINE('',#13350,#3187);
#2558=LINE('',#13352,#3188);
#2559=LINE('',#13353,#3189);
#2560=LINE('',#13358,#3190);
#2561=LINE('',#13360,#3191);
#2562=LINE('',#13362,#3192);
#2563=LINE('',#13364,#3193);
#2564=LINE('',#13366,#3194);
#2565=LINE('',#13368,#3195);
#2566=LINE('',#13369,#3196);
#2567=LINE('',#13372,#3197);
#2568=LINE('',#13373,#3198);
#2569=LINE('',#13376,#3199);
#2570=LINE('',#13377,#3200);
#2571=LINE('',#13380,#3201);
#2572=LINE('',#13382,#3202);
#2573=LINE('',#13384,#3203);
#2574=LINE('',#13386,#3204);
#2575=LINE('',#13387,#3205);
#2576=LINE('',#13389,#3206);
#2577=LINE('',#13392,#3207);
#2578=LINE('',#13395,#3208);
#2579=LINE('',#13399,#3209);
#2580=LINE('',#13406,#3210);
#2581=LINE('',#13408,#3211);
#2582=LINE('',#13410,#3212);
#3180=VECTOR('',#10767,1.);
#3181=VECTOR('',#10768,1.);
#3182=VECTOR('',#10769,1.);
#3183=VECTOR('',#10770,1.);
#3184=VECTOR('',#10773,1.);
#3185=VECTOR('',#10774,1.);
#3186=VECTOR('',#10775,1.);
#3187=VECTOR('',#10778,1.);
#3188=VECTOR('',#10779,1.);
#3189=VECTOR('',#10780,1.);
#3190=VECTOR('',#10785,1.);
#3191=VECTOR('',#10786,1.);
#3192=VECTOR('',#10787,1.);
#3193=VECTOR('',#10788,1.);
#3194=VECTOR('',#10789,1.);
#3195=VECTOR('',#10790,1.);
#3196=VECTOR('',#10791,1.);
#3197=VECTOR('',#10794,1.);
#3198=VECTOR('',#10795,1.);
#3199=VECTOR('',#10798,1.);
#3200=VECTOR('',#10799,1.);
#3201=VECTOR('',#10802,1.);
#3202=VECTOR('',#10803,1.);
#3203=VECTOR('',#10804,1.);
#3204=VECTOR('',#10805,1.);
#3205=VECTOR('',#10806,1.);
#3206=VECTOR('',#10809,1.);
#3207=VECTOR('',#10812,1.);
#3208=VECTOR('',#10815,1.);
#3209=VECTOR('',#10820,0.21);
#3210=VECTOR('',#10829,1.);
#3211=VECTOR('',#10832,1.);
#3212=VECTOR('',#10835,1.);
#3625=CIRCLE('',#9112,0.2117);
#3626=CIRCLE('',#9121,0.2117);
#3627=CIRCLE('',#9122,0.2117);
#3628=CIRCLE('',#9124,0.2117);
#4161=VERTEX_POINT('',#13334);
#4162=VERTEX_POINT('',#13335);
#4163=VERTEX_POINT('',#13337);
#4164=VERTEX_POINT('',#13339);
#4165=VERTEX_POINT('',#13343);
#4166=VERTEX_POINT('',#13345);
#4167=VERTEX_POINT('',#13349);
#4168=VERTEX_POINT('',#13351);
#4169=VERTEX_POINT('',#13354);
#4170=VERTEX_POINT('',#13357);
#4171=VERTEX_POINT('',#13359);
#4172=VERTEX_POINT('',#13361);
#4173=VERTEX_POINT('',#13363);
#4174=VERTEX_POINT('',#13365);
#4175=VERTEX_POINT('',#13367);
#4176=VERTEX_POINT('',#13371);
#4177=VERTEX_POINT('',#13375);
#4178=VERTEX_POINT('',#13379);
#4179=VERTEX_POINT('',#13381);
#4180=VERTEX_POINT('',#13383);
#4181=VERTEX_POINT('',#13385);
#4182=VERTEX_POINT('',#13391);
#4183=VERTEX_POINT('',#13393);
#4184=VERTEX_POINT('',#13397);
#4185=VERTEX_POINT('',#13400);
#4186=VERTEX_POINT('',#13402);
#4998=EDGE_CURVE('',#4161,#4162,#2550,.T.);
#4999=EDGE_CURVE('',#4163,#4161,#2551,.T.);
#5000=EDGE_CURVE('',#4164,#4163,#2552,.T.);
#5001=EDGE_CURVE('',#4162,#4164,#2553,.T.);
#5002=EDGE_CURVE('',#4163,#4165,#2554,.T.);
#5003=EDGE_CURVE('',#4166,#4165,#2555,.T.);
#5004=EDGE_CURVE('',#4164,#4166,#2556,.T.);
#5005=EDGE_CURVE('',#4165,#4167,#2557,.T.);
#5006=EDGE_CURVE('',#4167,#4168,#2558,.T.);
#5007=EDGE_CURVE('',#4168,#4166,#2559,.T.);
#5008=EDGE_CURVE('',#4169,#4169,#3625,.T.);
#5009=EDGE_CURVE('',#4170,#4161,#2560,.T.);
#5010=EDGE_CURVE('',#4171,#4170,#2561,.T.);
#5011=EDGE_CURVE('',#4171,#4172,#2562,.T.);
#5012=EDGE_CURVE('',#4173,#4172,#2563,.T.);
#5013=EDGE_CURVE('',#4173,#4174,#2564,.T.);
#5014=EDGE_CURVE('',#4174,#4175,#2565,.T.);
#5015=EDGE_CURVE('',#4175,#4167,#2566,.T.);
#5016=EDGE_CURVE('',#4175,#4176,#2567,.T.);
#5017=EDGE_CURVE('',#4176,#4168,#2568,.T.);
#5018=EDGE_CURVE('',#4177,#4174,#2569,.T.);
#5019=EDGE_CURVE('',#4176,#4177,#2570,.T.);
#5020=EDGE_CURVE('',#4178,#4177,#2571,.T.);
#5021=EDGE_CURVE('',#4179,#4178,#2572,.T.);
#5022=EDGE_CURVE('',#4179,#4180,#2573,.T.);
#5023=EDGE_CURVE('',#4181,#4180,#2574,.T.);
#5024=EDGE_CURVE('',#4181,#4162,#2575,.T.);
#5025=EDGE_CURVE('',#4178,#4173,#2576,.T.);
#5026=EDGE_CURVE('',#4172,#4182,#2577,.T.);
#5027=EDGE_CURVE('',#4182,#4183,#427,.T.);
#5028=EDGE_CURVE('',#4183,#4179,#2578,.T.);
#5029=EDGE_CURVE('',#4184,#4182,#3626,.F.);
#5030=EDGE_CURVE('',#4184,#4169,#2579,.T.);
#5031=EDGE_CURVE('',#4185,#4184,#3627,.F.);
#5032=EDGE_CURVE('',#4186,#4185,#428,.T.);
#5033=EDGE_CURVE('',#4183,#4186,#3628,.F.);
#5034=EDGE_CURVE('',#4185,#4171,#2580,.T.);
#5035=EDGE_CURVE('',#4180,#4186,#2581,.T.);
#5036=EDGE_CURVE('',#4170,#4181,#2582,.T.);
#6475=ORIENTED_EDGE('',*,*,#4998,.F.);
#6476=ORIENTED_EDGE('',*,*,#4999,.F.);
#6477=ORIENTED_EDGE('',*,*,#5000,.F.);
#6478=ORIENTED_EDGE('',*,*,#5001,.F.);
#6479=ORIENTED_EDGE('',*,*,#5000,.T.);
#6480=ORIENTED_EDGE('',*,*,#5002,.T.);
#6481=ORIENTED_EDGE('',*,*,#5003,.F.);
#6482=ORIENTED_EDGE('',*,*,#5004,.F.);
#6483=ORIENTED_EDGE('',*,*,#5005,.T.);
#6484=ORIENTED_EDGE('',*,*,#5006,.T.);
#6485=ORIENTED_EDGE('',*,*,#5007,.T.);
#6486=ORIENTED_EDGE('',*,*,#5003,.T.);
#6487=ORIENTED_EDGE('',*,*,#5008,.T.);
#6488=ORIENTED_EDGE('',*,*,#5005,.F.);
#6489=ORIENTED_EDGE('',*,*,#5002,.F.);
#6490=ORIENTED_EDGE('',*,*,#4999,.T.);
#6491=ORIENTED_EDGE('',*,*,#5009,.F.);
#6492=ORIENTED_EDGE('',*,*,#5010,.F.);
#6493=ORIENTED_EDGE('',*,*,#5011,.T.);
#6494=ORIENTED_EDGE('',*,*,#5012,.F.);
#6495=ORIENTED_EDGE('',*,*,#5013,.T.);
#6496=ORIENTED_EDGE('',*,*,#5014,.T.);
#6497=ORIENTED_EDGE('',*,*,#5015,.T.);
#6498=ORIENTED_EDGE('',*,*,#5016,.T.);
#6499=ORIENTED_EDGE('',*,*,#5017,.T.);
#6500=ORIENTED_EDGE('',*,*,#5006,.F.);
#6501=ORIENTED_EDGE('',*,*,#5015,.F.);
#6502=ORIENTED_EDGE('',*,*,#5018,.F.);
#6503=ORIENTED_EDGE('',*,*,#5019,.F.);
#6504=ORIENTED_EDGE('',*,*,#5016,.F.);
#6505=ORIENTED_EDGE('',*,*,#5014,.F.);
#6506=ORIENTED_EDGE('',*,*,#5007,.F.);
#6507=ORIENTED_EDGE('',*,*,#5017,.F.);
#6508=ORIENTED_EDGE('',*,*,#5019,.T.);
#6509=ORIENTED_EDGE('',*,*,#5020,.F.);
#6510=ORIENTED_EDGE('',*,*,#5021,.F.);
#6511=ORIENTED_EDGE('',*,*,#5022,.T.);
#6512=ORIENTED_EDGE('',*,*,#5023,.F.);
#6513=ORIENTED_EDGE('',*,*,#5024,.T.);
#6514=ORIENTED_EDGE('',*,*,#5001,.T.);
#6515=ORIENTED_EDGE('',*,*,#5004,.T.);
#6516=ORIENTED_EDGE('',*,*,#5018,.T.);
#6517=ORIENTED_EDGE('',*,*,#5013,.F.);
#6518=ORIENTED_EDGE('',*,*,#5025,.F.);
#6519=ORIENTED_EDGE('',*,*,#5020,.T.);
#6520=ORIENTED_EDGE('',*,*,#5021,.T.);
#6521=ORIENTED_EDGE('',*,*,#5025,.T.);
#6522=ORIENTED_EDGE('',*,*,#5012,.T.);
#6523=ORIENTED_EDGE('',*,*,#5026,.T.);
#6524=ORIENTED_EDGE('',*,*,#5027,.T.);
#6525=ORIENTED_EDGE('',*,*,#5028,.T.);
#6526=ORIENTED_EDGE('',*,*,#5027,.F.);
#6527=ORIENTED_EDGE('',*,*,#5029,.F.);
#6528=ORIENTED_EDGE('',*,*,#5030,.T.);
#6529=ORIENTED_EDGE('',*,*,#5008,.F.);
#6530=ORIENTED_EDGE('',*,*,#5030,.F.);
#6531=ORIENTED_EDGE('',*,*,#5031,.F.);
#6532=ORIENTED_EDGE('',*,*,#5032,.F.);
#6533=ORIENTED_EDGE('',*,*,#5033,.F.);
#6534=ORIENTED_EDGE('',*,*,#5026,.F.);
#6535=ORIENTED_EDGE('',*,*,#5011,.F.);
#6536=ORIENTED_EDGE('',*,*,#5034,.F.);
#6537=ORIENTED_EDGE('',*,*,#5031,.T.);
#6538=ORIENTED_EDGE('',*,*,#5029,.T.);
#6539=ORIENTED_EDGE('',*,*,#5028,.F.);
#6540=ORIENTED_EDGE('',*,*,#5033,.T.);
#6541=ORIENTED_EDGE('',*,*,#5035,.F.);
#6542=ORIENTED_EDGE('',*,*,#5022,.F.);
#6543=ORIENTED_EDGE('',*,*,#5010,.T.);
#6544=ORIENTED_EDGE('',*,*,#5036,.T.);
#6545=ORIENTED_EDGE('',*,*,#5023,.T.);
#6546=ORIENTED_EDGE('',*,*,#5035,.T.);
#6547=ORIENTED_EDGE('',*,*,#5032,.T.);
#6548=ORIENTED_EDGE('',*,*,#5034,.T.);
#6549=ORIENTED_EDGE('',*,*,#4998,.T.);
#6550=ORIENTED_EDGE('',*,*,#5024,.F.);
#6551=ORIENTED_EDGE('',*,*,#5036,.F.);
#6552=ORIENTED_EDGE('',*,*,#5009,.T.);
#7684=CYLINDRICAL_SURFACE('',#9120,0.2117);
#7955=ADVANCED_FACE('',(#1283),#912,.F.);
#7956=ADVANCED_FACE('',(#1284),#913,.T.);
#7957=ADVANCED_FACE('',(#1285,#716),#914,.T.);
#7958=ADVANCED_FACE('',(#1286),#915,.T.);
#7959=ADVANCED_FACE('',(#1287),#916,.T.);
#7960=ADVANCED_FACE('',(#1288),#917,.F.);
#7961=ADVANCED_FACE('',(#1289),#918,.T.);
#7962=ADVANCED_FACE('',(#1290),#919,.T.);
#7963=ADVANCED_FACE('',(#1291),#920,.T.);
#7964=ADVANCED_FACE('',(#1292),#7684,.F.);
#7965=ADVANCED_FACE('',(#1293),#921,.F.);
#7966=ADVANCED_FACE('',(#1294),#922,.F.);
#7967=ADVANCED_FACE('',(#1295),#923,.T.);
#7968=ADVANCED_FACE('',(#1296),#924,.T.);
#8258=CLOSED_SHELL('',(#7955,#7956,#7957,#7958,#7959,#7960,#7961,#7962,
#7963,#7964,#7965,#7966,#7967,#7968));
#9108=AXIS2_PLACEMENT_3D('',#13332,#10763,#10764);
#9109=AXIS2_PLACEMENT_3D('',#13333,#10765,#10766);
#9110=AXIS2_PLACEMENT_3D('',#13342,#10771,#10772);
#9111=AXIS2_PLACEMENT_3D('',#13348,#10776,#10777);
#9112=AXIS2_PLACEMENT_3D('',#13355,#10781,#10782);
#9113=AXIS2_PLACEMENT_3D('',#13356,#10783,#10784);
#9114=AXIS2_PLACEMENT_3D('',#13370,#10792,#10793);
#9115=AXIS2_PLACEMENT_3D('',#13374,#10796,#10797);
#9116=AXIS2_PLACEMENT_3D('',#13378,#10800,#10801);
#9117=AXIS2_PLACEMENT_3D('',#13388,#10807,#10808);
#9118=AXIS2_PLACEMENT_3D('',#13390,#10810,#10811);
#9119=AXIS2_PLACEMENT_3D('',#13394,#10813,#10814);
#9120=AXIS2_PLACEMENT_3D('',#13396,#10816,#10817);
#9121=AXIS2_PLACEMENT_3D('',#13398,#10818,#10819);
#9122=AXIS2_PLACEMENT_3D('',#13401,#10821,#10822);
#9123=AXIS2_PLACEMENT_3D('',#13403,#10823,#10824);
#9124=AXIS2_PLACEMENT_3D('',#13404,#10825,#10826);
#9125=AXIS2_PLACEMENT_3D('',#13405,#10827,#10828);
#9126=AXIS2_PLACEMENT_3D('',#13407,#10830,#10831);
#9127=AXIS2_PLACEMENT_3D('',#13409,#10833,#10834);
#9128=AXIS2_PLACEMENT_3D('',#13411,#10836,#10837);
#10763=DIRECTION('axis',(0.,0.,1.));
#10764=DIRECTION('refdir',(1.,0.,0.));
#10765=DIRECTION('center_axis',(0.,0.,1.));
#10766=DIRECTION('ref_axis',(1.,0.,0.));
#10767=DIRECTION('',(1.,0.,0.));
#10768=DIRECTION('',(0.,-1.,0.));
#10769=DIRECTION('',(-1.,0.,0.));
#10770=DIRECTION('',(0.,1.,0.));
#10771=DIRECTION('center_axis',(0.,1.,0.));
#10772=DIRECTION('ref_axis',(-1.,0.,0.));
#10773=DIRECTION('',(0.,0.,1.));
#10774=DIRECTION('',(-1.,0.,0.));
#10775=DIRECTION('',(0.,0.,1.));
#10776=DIRECTION('center_axis',(0.,0.,1.));
#10777=DIRECTION('ref_axis',(1.,0.,0.));
#10778=DIRECTION('',(0.,-1.,0.));
#10779=DIRECTION('',(1.,0.,0.));
#10780=DIRECTION('',(0.,1.,0.));
#10781=DIRECTION('center_axis',(0.,0.,-1.));
#10782=DIRECTION('ref_axis',(1.,0.,0.));
#10783=DIRECTION('center_axis',(-1.,0.,0.));
#10784=DIRECTION('ref_axis',(0.,-1.,0.));
#10785=DIRECTION('',(0.,0.,1.));
#10786=DIRECTION('',(0.,0.707106781186548,0.707106781186548));
#10787=DIRECTION('',(0.,-1.,0.));
#10788=DIRECTION('',(0.,0.707106781186548,-0.707106781186548));
#10789=DIRECTION('',(0.,0.,1.));
#10790=DIRECTION('',(0.,-1.,0.));
#10791=DIRECTION('',(0.,0.,1.));
#10792=DIRECTION('center_axis',(0.,-1.,0.));
#10793=DIRECTION('ref_axis',(1.,0.,0.));
#10794=DIRECTION('',(1.,0.,0.));
#10795=DIRECTION('',(0.,0.,1.));
#10796=DIRECTION('center_axis',(0.,0.,1.));
#10797=DIRECTION('ref_axis',(1.,0.,0.));
#10798=DIRECTION('',(-1.,0.,0.));
#10799=DIRECTION('',(0.,1.,0.));
#10800=DIRECTION('center_axis',(1.,0.,0.));
#10801=DIRECTION('ref_axis',(0.,1.,0.));
#10802=DIRECTION('',(0.,0.,1.));
#10803=DIRECTION('',(0.,-0.707106781186548,0.707106781186548));
#10804=DIRECTION('',(0.,1.,0.));
#10805=DIRECTION('',(0.,-0.707106781186548,-0.707106781186548));
#10806=DIRECTION('',(0.,0.,1.));
#10807=DIRECTION('center_axis',(0.,-1.,0.));
#10808=DIRECTION('ref_axis',(1.,0.,0.));
#10809=DIRECTION('',(-1.,0.,0.));
#10810=DIRECTION('center_axis',(0.,-0.707106781186548,-0.707106781186548));
#10811=DIRECTION('ref_axis',(-1.,0.,0.));
#10812=DIRECTION('',(1.,0.,0.));
#10813=DIRECTION('center_axis',(0.,0.707106781186548,0.707106781186548));
#10814=DIRECTION('ref_axis',(0.,0.707106781186547,-0.707106781186547));
#10815=DIRECTION('',(1.,0.,0.));
#10816=DIRECTION('center_axis',(0.,0.,1.));
#10817=DIRECTION('ref_axis',(1.,0.,0.));
#10818=DIRECTION('center_axis',(0.,0.,-1.));
#10819=DIRECTION('ref_axis',(1.,0.,0.));
#10820=DIRECTION('',(0.,0.,1.));
#10821=DIRECTION('center_axis',(0.,0.,-1.));
#10822=DIRECTION('ref_axis',(1.,0.,0.));
#10823=DIRECTION('center_axis',(0.,-0.707106781186548,0.707106781186548));
#10824=DIRECTION('ref_axis',(0.,0.707106781186547,0.707106781186547));
#10825=DIRECTION('center_axis',(0.,0.,-1.));
#10826=DIRECTION('ref_axis',(1.,0.,0.));
#10827=DIRECTION('center_axis',(0.,0.,1.));
#10828=DIRECTION('ref_axis',(1.,0.,0.));
#10829=DIRECTION('',(-1.,0.,0.));
#10830=DIRECTION('center_axis',(0.,0.,1.));
#10831=DIRECTION('ref_axis',(1.,0.,0.));
#10832=DIRECTION('',(-1.,0.,0.));
#10833=DIRECTION('center_axis',(0.,0.707106781186548,-0.707106781186548));
#10834=DIRECTION('ref_axis',(-1.,0.,0.));
#10835=DIRECTION('',(1.,0.,0.));
#10836=DIRECTION('center_axis',(0.,1.,0.));
#10837=DIRECTION('ref_axis',(-1.,0.,0.));
#13332=CARTESIAN_POINT('',(0.,0.,0.));
#13333=CARTESIAN_POINT('Origin',(0.,0.395,0.25));
#13334=CARTESIAN_POINT('',(-0.5,0.3,0.25));
#13335=CARTESIAN_POINT('',(0.5,0.3,0.25));
#13336=CARTESIAN_POINT('',(0.25,0.3,0.25));
#13337=CARTESIAN_POINT('',(-0.5,0.5,0.25));
#13338=CARTESIAN_POINT('',(-0.5,0.5,0.25));
#13339=CARTESIAN_POINT('',(0.5,0.5,0.25));
#13340=CARTESIAN_POINT('',(0.5,0.5,0.25));
#13341=CARTESIAN_POINT('',(0.5,0.29,0.25));
#13342=CARTESIAN_POINT('Origin',(0.5,0.5,0.25));
#13343=CARTESIAN_POINT('',(-0.5,0.5,0.4));
#13344=CARTESIAN_POINT('',(-0.5,0.5,0.25));
#13345=CARTESIAN_POINT('',(0.5,0.5,0.4));
#13346=CARTESIAN_POINT('',(0.5,0.5,0.4));
#13347=CARTESIAN_POINT('',(0.5,0.5,0.25));
#13348=CARTESIAN_POINT('Origin',(0.,0.,0.4));
#13349=CARTESIAN_POINT('',(-0.5,-0.5,0.4));
#13350=CARTESIAN_POINT('',(-0.5,0.5,0.4));
#13351=CARTESIAN_POINT('',(0.5,-0.5,0.4));
#13352=CARTESIAN_POINT('',(-0.5,-0.5,0.4));
#13353=CARTESIAN_POINT('',(0.5,-0.3,0.4));
#13354=CARTESIAN_POINT('',(-0.2117,2.59257727379495E-17,0.4));
#13355=CARTESIAN_POINT('Origin',(0.,0.,0.4));
#13356=CARTESIAN_POINT('Origin',(-0.5,0.3,0.));
#13357=CARTESIAN_POINT('',(-0.5,0.3,0.15));
#13358=CARTESIAN_POINT('',(-0.5,0.3,0.));
#13359=CARTESIAN_POINT('',(-0.5,0.15,0.));
#13360=CARTESIAN_POINT('',(-0.5,0.225,0.075));
#13361=CARTESIAN_POINT('',(-0.5,-0.15,0.));
#13362=CARTESIAN_POINT('',(-0.5,0.3,0.));
#13363=CARTESIAN_POINT('',(-0.5,-0.3,0.15));
#13364=CARTESIAN_POINT('',(-0.5,-0.075,-0.075));
#13365=CARTESIAN_POINT('',(-0.5,-0.3,0.25));
#13366=CARTESIAN_POINT('',(-0.5,-0.3,0.));
#13367=CARTESIAN_POINT('',(-0.5,-0.5,0.25));
#13368=CARTESIAN_POINT('',(-0.5,-0.29,0.25));
#13369=CARTESIAN_POINT('',(-0.5,-0.5,0.25));
#13370=CARTESIAN_POINT('Origin',(-0.5,-0.5,0.25));
#13371=CARTESIAN_POINT('',(0.5,-0.5,0.25));
#13372=CARTESIAN_POINT('',(-0.5,-0.5,0.25));
#13373=CARTESIAN_POINT('',(0.5,-0.5,0.25));
#13374=CARTESIAN_POINT('Origin',(0.,-0.395,0.25));
#13375=CARTESIAN_POINT('',(0.5,-0.3,0.25));
#13376=CARTESIAN_POINT('',(-0.25,-0.3,0.25));
#13377=CARTESIAN_POINT('',(0.5,-0.5,0.25));
#13378=CARTESIAN_POINT('Origin',(0.5,-0.3,0.));
#13379=CARTESIAN_POINT('',(0.5,-0.3,0.15));
#13380=CARTESIAN_POINT('',(0.5,-0.3,0.));
#13381=CARTESIAN_POINT('',(0.5,-0.15,0.));
#13382=CARTESIAN_POINT('',(0.5,-0.225,0.075));
#13383=CARTESIAN_POINT('',(0.5,0.15,0.));
#13384=CARTESIAN_POINT('',(0.5,-0.3,0.));
#13385=CARTESIAN_POINT('',(0.5,0.3,0.15));
#13386=CARTESIAN_POINT('',(0.5,0.075,-0.075));
#13387=CARTESIAN_POINT('',(0.5,0.3,0.));
#13388=CARTESIAN_POINT('Origin',(-0.5,-0.3,0.));
#13389=CARTESIAN_POINT('',(-0.25,-0.3,0.15));
#13390=CARTESIAN_POINT('Origin',(-0.25,-0.225,0.075));
#13391=CARTESIAN_POINT('',(-0.149388386429468,-0.15,0.));
#13392=CARTESIAN_POINT('',(-0.25,-0.15,0.));
#13393=CARTESIAN_POINT('',(0.149388386429468,-0.15,0.));
#13394=CARTESIAN_POINT('Origin',(0.,0.,-0.15));
#13395=CARTESIAN_POINT('',(-0.25,-0.15,0.));
#13396=CARTESIAN_POINT('Origin',(0.,0.,-0.1));
#13397=CARTESIAN_POINT('',(-0.2117,-2.59257727379495E-17,0.));
#13398=CARTESIAN_POINT('Origin',(0.,0.,0.));
#13399=CARTESIAN_POINT('',(-0.2117,-2.59257727379495E-17,-0.1));
#13400=CARTESIAN_POINT('',(-0.149388386429468,0.15,0.));
#13401=CARTESIAN_POINT('Origin',(0.,0.,0.));
#13402=CARTESIAN_POINT('',(0.149388386429468,0.15,0.));
#13403=CARTESIAN_POINT('Origin',(0.,0.,-0.15));
#13404=CARTESIAN_POINT('Origin',(0.,0.,0.));
#13405=CARTESIAN_POINT('Origin',(0.,0.,0.));
#13406=CARTESIAN_POINT('',(0.25,0.15,0.));
#13407=CARTESIAN_POINT('Origin',(0.,0.,0.));
#13408=CARTESIAN_POINT('',(0.25,0.15,0.));
#13409=CARTESIAN_POINT('Origin',(0.25,0.225,0.075));
#13410=CARTESIAN_POINT('',(0.25,0.3,0.15));
#13411=CARTESIAN_POINT('Origin',(0.5,0.3,0.));
#15128=UNCERTAINTY_MEASURE_WITH_UNIT(LENGTH_MEASURE(0.001),#15213,
'DISTANCE_ACCURACY_VALUE',
'Maximum model space distance between geometric entities at asserted c
onnectivities');
#15162=UNCERTAINTY_MEASURE_WITH_UNIT(LENGTH_MEASURE(0.001),#15213,
'DISTANCE_ACCURACY_VALUE',
'Maximum model space distance between geometric entities at asserted c
onnectivities');
#15178=(
GEOMETRIC_REPRESENTATION_CONTEXT(3)
GLOBAL_UNCERTAINTY_ASSIGNED_CONTEXT((#15128))
GLOBAL_UNIT_ASSIGNED_CONTEXT((#15213,#15215,#15216))
REPRESENTATION_CONTEXT('','3D')
);
#15212=(
GEOMETRIC_REPRESENTATION_CONTEXT(3)
GLOBAL_UNCERTAINTY_ASSIGNED_CONTEXT((#15162))
GLOBAL_UNIT_ASSIGNED_CONTEXT((#15213,#15215,#15216))
REPRESENTATION_CONTEXT('','3D')
);
#15213=(
LENGTH_UNIT()
NAMED_UNIT(*)
SI_UNIT(.CENTI.,.METRE.)
);
#15215=(
NAMED_UNIT(*)
PLANE_ANGLE_UNIT()
SI_UNIT($,.RADIAN.)
);
#15216=(
NAMED_UNIT(*)
SI_UNIT($,.STERADIAN.)
SOLID_ANGLE_UNIT()
);
#15232=SHAPE_DEFINITION_REPRESENTATION(#15281,#15416);
#15281=PRODUCT_DEFINITION_SHAPE('',$,#15466);
#15416=SHAPE_REPRESENTATION('',(#9108),#15178);
#15450=PRODUCT_DEFINITION_CONTEXT('part definition',#15599,'design');
#15466=PRODUCT_DEFINITION('Captive slot nut','Captive slot nut',#15515,
#15450);
#15515=PRODUCT_DEFINITION_FORMATION('',$,#15616);
#15599=APPLICATION_CONTEXT(
'Core Data for Automotive Mechanical Design Process');
#15600=PRODUCT_CONTEXT('part definition',#15599,'mechanical');
#15616=PRODUCT('Captive slot nut','Captive slot nut','Captive slot nut',
(#15600));
#15720=COLOUR_RGB('Black',0.12,0.14,0.17);
#15721=FILL_AREA_STYLE_COLOUR('',#15720);
#15722=FILL_AREA_STYLE('',(#15721));
#15723=SURFACE_STYLE_FILL_AREA(#15722);
#15724=SURFACE_SIDE_STYLE('',(#15723));
#15725=SURFACE_STYLE_USAGE(.BOTH.,#15724);
#15726=PRESENTATION_STYLE_ASSIGNMENT((#15725));
ENDSEC;
END-ISO-10303-21;
